ISO-10303-21;
HEADER;
FILE_DESCRIPTION (('STEP AP214'),
    '1' );
FILE_NAME ('socket head cap screw_iso_ISO 4762 M5 x 16 - 16N.step',
    '2026-10-27T17:01:19',
    ( '' ),
    ( '' ),
    'SwSTEP 2.0',
    'SolidWorks 2026',
    '' );
FILE_SCHEMA (( 'AUTOMOTIVE_DESIGN' ));
ENDSEC;

DATA;
#1=AXIS2_PLACEMENT_3D ( 'NONE', #9053, #14371, #13552 ) ;
#10=DIRECTION ( 'NONE',  ( 0.000000000000000000, 0.000000000000000000, -1.000000000000000000 ) ) ;
#19=TOROIDAL_SURFACE ( 'NONE', #6418, 2.700000000000000622, 0.2000000000000000111 ) ;
#66=DIRECTION ( 'NONE',  ( 0.000000000000000000, 0.000000000000000000, 1.000000000000000000 ) ) ;
#147=DIRECTION ( 'NONE',  ( 0.000000000000000000, 0.000000000000000000, 1.000000000000000000 ) ) ;
#158=VECTOR ( 'NONE', #9040, 1000.000000000000000 ) ;
#182=CIRCLE ( 'NONE', #10114, 0.2000000000000000944 ) ;
#190=FACE_OUTER_BOUND ( 'NONE', #11579, .T. ) ;
#193=EDGE_LOOP ( 'NONE', ( #2834, #237, #12964, #6241 ) ) ;
#221=AXIS2_PLACEMENT_3D ( 'NONE', #1029, #9011, #10110 ) ;
#225=VECTOR ( 'NONE', #9137, 1000.000000000000114 ) ;
#237=ORIENTED_EDGE ( 'NONE', *, *, #8274, .T. ) ;
#241=VECTOR ( 'NONE', #10180, 1000.000000000000000 ) ;
#269=ORIENTED_EDGE ( 'NONE', *, *, #1906, .F. ) ;
#271=CARTESIAN_POINT ( 'NONE',  ( 21.00000000000000355, 0.000000000000000000, 0.000000000000000000 ) ) ;
#312=CARTESIAN_POINT ( 'NONE',  ( 2.500000000000000000, 0.000000000000000000, 2.041999999999999815 ) ) ;
#350=CARTESIAN_POINT ( 'NONE',  ( -31.74999999999995737, 0.000000000000000000, 0.000000000000000000 ) ) ;
#351=DIRECTION ( 'NONE',  ( 1.000000000000000000, 0.000000000000000000, 0.000000000000000000 ) ) ;
#371=SURFACE_SIDE_STYLE ('',( #5065 ) ) ;
#408=AXIS2_PLACEMENT_3D ( 'NONE', #8734, #14339, #4160 ) ;
#423=ORIENTED_EDGE ( 'NONE', *, *, #14433, .T. ) ;
#431=CYLINDRICAL_SURFACE ( 'NONE', #1910, 2.500000000000000444 ) ;
#445=LINE ( 'NONE', #3798, #12275 ) ;
#460=PRESENTATION_STYLE_ASSIGNMENT (( #13912 ) ) ;
#464=EDGE_LOOP ( 'NONE', ( #13550, #7298, #1081, #14367, #9669 ) ) ;
#465=ORIENTED_EDGE ( 'NONE', *, *, #873, .F. ) ;
#518=EDGE_CURVE ( 'NONE', #809, #9573, #9326, .T. ) ;
#569=EDGE_LOOP ( 'NONE', ( #3995, #1512, #2754, #4676 ) ) ;
#598=CARTESIAN_POINT ( 'NONE',  ( 5.000000000000000888, 0.000000000000000000, 0.000000000000000000 ) ) ;
#599=CARTESIAN_POINT ( 'NONE',  ( 2.500000000000000000, -1.178949249685214307, 2.042000000000001592 ) ) ;
#612=DIRECTION ( 'NONE',  ( 0.000000000000000000, 0.000000000000000000, -1.000000000000000000 ) ) ;
#663=AXIS2_PLACEMENT_3D ( 'NONE', #6729, #1108, #5622 ) ;
#706=ORIENTED_EDGE ( 'NONE', *, *, #5865, .T. ) ;
#717=ORIENTED_EDGE ( 'NONE', *, *, #3635, .T. ) ;
#736=CARTESIAN_POINT ( 'NONE',  ( 0.000000000000000000, 1.178949249685212974, -2.042000000000001148 ) ) ;
#758=ORIENTED_EDGE ( 'NONE', *, *, #8000, .T. ) ;
#774=CARTESIAN_POINT ( 'NONE',  ( 21.00000000000000355, 0.000000000000000000, 0.000000000000000000 ) ) ;
#783=VERTEX_POINT ( 'NONE', #5601 ) ;
#806=LINE ( 'NONE', #13005, #9213 ) ;
#809=VERTEX_POINT ( 'NONE', #3324 ) ;
#822=CARTESIAN_POINT ( 'NONE',  ( 2.500000000000000000, -1.178949249685214307, 2.042000000000001592 ) ) ;
#825=EDGE_LOOP ( 'NONE', ( #10283, #10217, #7029, #3003, #5201 ) ) ;
#873=EDGE_CURVE ( 'NONE', #5188, #11030, #8324, .T. ) ;
#874=CARTESIAN_POINT ( 'NONE',  ( -31.74999999999995737, 5.204748896376250699E-16, -4.250000000000000000 ) ) ;
#879=CARTESIAN_POINT ( 'NONE',  ( 0.2500000000000002220, 0.000000000000000000, 4.250000000000000000 ) ) ;
#888=DIRECTION ( 'NONE',  ( 0.000000000000000000, 0.000000000000000000, -1.000000000000000000 ) ) ;
#891=EDGE_LOOP ( 'NONE', ( #13342, #8061 ) ) ;
#927=DIRECTION ( 'NONE',  ( -0.000000000000000000, 1.287488025362403787E-15, 1.000000000000000000 ) ) ;
#939=VECTOR ( 'NONE', #5652, 1000.000000000000114 ) ;
#946=EDGE_LOOP ( 'NONE', ( #1927, #13007, #3198 ) ) ;
#949=DIRECTION ( 'NONE',  ( 0.000000000000000000, 0.000000000000000000, 1.000000000000000000 ) ) ;
#969=ORIENTED_EDGE ( 'NONE', *, *, #5757, .F. ) ;
#972=PRODUCT_DEFINITION ( 'UNKNOWN', '', #3122, #9597 ) ;
#973=CARTESIAN_POINT ( 'NONE',  ( 21.00000000000000355, 2.789133085058097101E-16, -2.055000000000000160 ) ) ;
#1007=DIRECTION ( 'NONE',  ( -1.000000000000000000, -0.000000000000000000, -0.000000000000000000 ) ) ;
#1018=LINE ( 'NONE', #10987, #13459 ) ;
#1028=SHAPE_DEFINITION_REPRESENTATION ( #6637, #12910 ) ;
#1029=CARTESIAN_POINT ( 'NONE',  ( 2.500000000000000000, 2.357898499370431722, -2.818925648462311528E-15 ) ) ;
#1081=ORIENTED_EDGE ( 'NONE', *, *, #4008, .T. ) ;
#1088=CARTESIAN_POINT ( 'NONE',  ( 21.00000000000000355, 2.516649172247811061E-16, -2.055000000000000160 ) ) ;
#1105=STYLED_ITEM('',(#14681),#2215);
#1108=DIRECTION ( 'NONE',  ( 1.000000000000000000, 0.000000000000000000, 0.000000000000000000 ) ) ;
#1118=VECTOR ( 'NONE', #1505, 1000.000000000000114 ) ;
#1134=CIRCLE ( 'NONE', #11736, 2.041999999999999815 ) ;
#1135=VERTEX_POINT ( 'NONE', #1352 ) ;
#1139=CARTESIAN_POINT ( 'NONE',  ( -31.74999999999995737, 0.000000000000000000, 0.000000000000000000 ) ) ;
#1151=ADVANCED_FACE ( 'NONE', ( #13542 ), #5638, .F. ) ;
#1180=CIRCLE ( 'NONE', #3319, 2.700000000000000622 ) ;
#1191=ADVANCED_FACE ( 'NONE', ( #7929 ), #11961, .F. ) ;
#1224=CARTESIAN_POINT ( 'NONE',  ( 5.000000000000002665, 3.306546357697854226E-16, 2.700000000000000622 ) ) ;
#1266=CARTESIAN_POINT ( 'NONE',  ( 4.999999999999997335, 0.000000000000000000, 0.000000000000000000 ) ) ;
#1270=EDGE_CURVE ( 'NONE', #14191, #3125, #7474, .T. ) ;
#1298=ORIENTED_EDGE ( 'NONE', *, *, #3771, .T. ) ;
#1317=CARTESIAN_POINT ( 'NONE',  ( -31.74999999999995737, 0.000000000000000000, 2.500000000000000444 ) ) ;
#1320=EDGE_CURVE ( 'NONE', #13064, #8019, #12802, .T. ) ;
#1324=VERTEX_POINT ( 'NONE', #8361 ) ;
#1351=CARTESIAN_POINT ( 'NONE',  ( 2.500000000000000000, 0.000000000000000000, 0.000000000000000000 ) ) ;
#1352=CARTESIAN_POINT ( 'NONE',  ( 0.000000000000000000, 1.178949249685212974, -2.042000000000001148 ) ) ;
#1395=EDGE_CURVE ( 'NONE', #5257, #4953, #9858, .T. ) ;
#1413=EDGE_CURVE ( 'NONE', #2369, #1324, #2296, .T. ) ;
#1424=AXIS2_PLACEMENT_3D ( 'NONE', #10126, #11383, #66 ) ;
#1485=FACE_OUTER_BOUND ( 'NONE', #946, .T. ) ;
#1505=DIRECTION ( 'NONE',  ( 0.000000000000000000, -0.5000000000000009992, -0.8660254037844380415 ) ) ;
#1512=ORIENTED_EDGE ( 'NONE', *, *, #4932, .T. ) ;
#1517=CARTESIAN_POINT ( 'NONE',  ( 2.500000000000000000, 2.357898499370431722, -2.818925648462311528E-15 ) ) ;
#1524=ORIENTED_EDGE ( 'NONE', *, *, #7166, .T. ) ;
#1569=FILL_AREA_STYLE_COLOUR ( '', #13720 ) ;
#1571=CARTESIAN_POINT ( 'NONE',  ( 4.999999999999997335, 0.000000000000000000, 4.250000000000000000 ) ) ;
#1572=ORIENTED_EDGE ( 'NONE', *, *, #12129, .F. ) ;
#1573=VERTEX_POINT ( 'NONE', #7852 ) ;
#1589=ORIENTED_EDGE ( 'NONE', *, *, #5597, .T. ) ;
#1599=AXIS2_PLACEMENT_3D ( 'NONE', #10361, #10440, #2618 ) ;
#1609=DIRECTION ( 'NONE',  ( 0.000000000000000000, 0.000000000000000000, 1.000000000000000000 ) ) ;
#1617=DIRECTION ( 'NONE',  ( -1.000000000000000000, -0.000000000000000000, -0.000000000000000000 ) ) ;
#1622=VECTOR ( 'NONE', #4145, 1000.000000000000000 ) ;
#1635=AXIS2_PLACEMENT_3D ( 'NONE', #14546, #8800, #9017 ) ;
#1636=ADVANCED_FACE ( 'NONE', ( #2286 ), #6541, .T. ) ;
#1644=CARTESIAN_POINT ( 'NONE',  ( 0.000000000000000000, 0.000000000000000000, 0.000000000000000000 ) ) ;
#1651=( NAMED_UNIT ( * ) PLANE_ANGLE_UNIT ( ) SI_UNIT ( $, .RADIAN. ) );
#1662=LINE ( 'NONE', #11756, #2513 ) ;
#1670=FACE_OUTER_BOUND ( 'NONE', #4542, .T. ) ;
#1671=PLANE ( 'NONE',  #5032 ) ;
#1691=CIRCLE ( 'NONE', #14422, 2.041999999999999815 ) ;
#1716=VERTEX_POINT ( 'NONE', #12628 ) ;
#1737=FACE_OUTER_BOUND ( 'NONE', #12077, .T. ) ;
#1753=DIRECTION ( 'NONE',  ( -1.000000000000000000, -0.000000000000000000, -0.000000000000000000 ) ) ;
#1760=EDGE_CURVE ( 'NONE', #14191, #12163, #1134, .T. ) ;
#1795=EDGE_LOOP ( 'NONE', ( #11184, #269, #706, #1589, #3816, #4469 ) ) ;
#1829=AXIS2_PLACEMENT_3D ( 'NONE', #13037, #2924, #7421 ) ;
#1846=ORIENTED_EDGE ( 'NONE', *, *, #5206, .F. ) ;
#1853=DIRECTION ( 'NONE',  ( 0.000000000000000000, 0.000000000000000000, 1.000000000000000000 ) ) ;
#1875=CARTESIAN_POINT ( 'NONE',  ( 0.000000000000000000, 0.000000000000000000, 4.000000000000000000 ) ) ;
#1879=AXIS2_PLACEMENT_3D ( 'NONE', #1351, #12641, #147 ) ;
#1886=ORIENTED_EDGE ( 'NONE', *, *, #5597, .F. ) ;
#1906=EDGE_CURVE ( 'NONE', #8019, #4246, #12164, .T. ) ;
#1910=AXIS2_PLACEMENT_3D ( 'NONE', #350, #8568, #2730 ) ;
#1927=ORIENTED_EDGE ( 'NONE', *, *, #5206, .T. ) ;
#1976=EDGE_CURVE ( 'NONE', #783, #5188, #12100, .T. ) ;
#1977=CARTESIAN_POINT ( 'NONE',  ( 2.500000000000000000, -1.178949249685214307, 2.042000000000001592 ) ) ;
#1978=ORIENTED_EDGE ( 'NONE', *, *, #8265, .F. ) ;
#1980=DIRECTION ( 'NONE',  ( -1.000000000000000000, -0.000000000000000000, -0.000000000000000000 ) ) ;
#1986=DIRECTION ( 'NONE',  ( -1.000000000000000000, -0.000000000000000000, -0.000000000000000000 ) ) ;
#2003=DIRECTION ( 'NONE',  ( 0.000000000000000000, -1.000000000000000000, 0.000000000000000000 ) ) ;
#2024=EDGE_LOOP ( 'NONE', ( #6218, #423, #4699, #6724 ) ) ;
#2052=CARTESIAN_POINT ( 'NONE',  ( 2.500000000000000000, 2.500728763858895382E-16, -2.041999999999999815 ) ) ;
#2053=CYLINDRICAL_SURFACE ( 'NONE', #10817, 2.500000000000000444 ) ;
#2150=EDGE_CURVE ( 'NONE', #4953, #5257, #7720, .T. ) ;
#2199=LINE ( 'NONE', #10024, #241 ) ;
#2215=MANIFOLD_SOLID_BREP ( 'Hex', #7630 ) ;
#2221=CARTESIAN_POINT ( 'NONE',  ( 21.00000000000000355, 0.000000000000000000, 0.000000000000000000 ) ) ;
#2222=PLANE ( 'NONE',  #663 ) ;
#2249=ORIENTED_EDGE ( 'NONE', *, *, #10270, .F. ) ;
#2286=FACE_OUTER_BOUND ( 'NONE', #2024, .T. ) ;
#2296=CIRCLE ( 'NONE', #12436, 2.500000000000000444 ) ;
#2324=CARTESIAN_POINT ( 'NONE',  ( 20.55500000000001748, 0.000000000000000000, 0.000000000000000000 ) ) ;
#2346=DIRECTION ( 'NONE',  ( 0.000000000000000000, 1.000000000000000000, -1.224646799147353207E-16 ) ) ;
#2367=CIRCLE ( 'NONE', #1424, 4.250000000000000000 ) ;
#2369=VERTEX_POINT ( 'NONE', #8440 ) ;
#2377=ORIENTED_EDGE ( 'NONE', *, *, #11620, .F. ) ;
#2381=ADVANCED_FACE ( 'NONE', ( #1737 ), #9636, .F. ) ;
#2396=( GEOMETRIC_REPRESENTATION_CONTEXT ( 3 ) GLOBAL_UNCERTAINTY_ASSIGNED_CONTEXT ( ( #9887 ) ) GLOBAL_UNIT_ASSIGNED_CONTEXT ( ( #4840, #9405, #3729 ) ) REPRESENTATION_CONTEXT ( 'NONE', 'WORKASPACE' ) );
#2461=DIRECTION ( 'NONE',  ( -0.000000000000000000, 0.000000000000000000, 1.000000000000000000 ) ) ;
#2506=DIRECTION ( 'NONE',  ( 0.000000000000000000, 0.000000000000000000, -1.000000000000000000 ) ) ;
#2513=VECTOR ( 'NONE', #11450, 1000.000000000000000 ) ;
#2610=CIRCLE ( 'NONE', #5916, 0.2500000000000002220 ) ;
#2618=DIRECTION ( 'NONE',  ( 0.000000000000000000, 1.000000000000000000, -1.287488025362403787E-15 ) ) ;
#2655=ORIENTED_EDGE ( 'NONE', *, *, #10016, .F. ) ;
#2664=DIRECTION ( 'NONE',  ( -1.000000000000000000, -0.000000000000000000, -0.000000000000000000 ) ) ;
#2697=EDGE_CURVE ( 'NONE', #9095, #4166, #11499, .T. ) ;
#2706=ORIENTED_EDGE ( 'NONE', *, *, #11506, .T. ) ;
#2718=EDGE_CURVE ( 'NONE', #13064, #12163, #13068, .T. ) ;
#2730=DIRECTION ( 'NONE',  ( 0.000000000000000000, 0.000000000000000000, 1.000000000000000000 ) ) ;
#2743=DIRECTION ( 'NONE',  ( 0.000000000000000000, 0.5000000000000009992, 0.8660254037844380415 ) ) ;
#2750=DIRECTION ( 'NONE',  ( 0.000000000000000000, -0.4999999999999989453, 0.8660254037844391517 ) ) ;
#2754=ORIENTED_EDGE ( 'NONE', *, *, #2150, .F. ) ;
#2760=VECTOR ( 'NONE', #7455, 1000.000000000000000 ) ;
#2772=FACE_BOUND ( 'NONE', #10036, .T. ) ;
#2791=CARTESIAN_POINT ( 'NONE',  ( 0.2500000000000002220, 0.000000000000000000, 0.000000000000000000 ) ) ;
#2829=CIRCLE ( 'NONE', #1879, 2.041999999999999815 ) ;
#2834=ORIENTED_EDGE ( 'NONE', *, *, #11620, .T. ) ;
#2878=DIRECTION ( 'NONE',  ( -1.000000000000000000, -0.000000000000000000, -0.000000000000000000 ) ) ;
#2924=DIRECTION ( 'NONE',  ( 1.000000000000000000, 0.000000000000000000, 0.000000000000000000 ) ) ;
#2944=EDGE_LOOP ( 'NONE', ( #1572, #13039 ) ) ;
#2974=DIRECTION ( 'NONE',  ( -1.000000000000000000, -0.000000000000000000, -0.000000000000000000 ) ) ;
#2983=ORIENTED_EDGE ( 'NONE', *, *, #10270, .T. ) ;
#2987=DIRECTION ( 'NONE',  ( 0.000000000000000000, -1.224646799147353454E-16, 1.000000000000000000 ) ) ;
#2994=DIRECTION ( 'NONE',  ( 0.000000000000000000, 0.000000000000000000, 1.000000000000000000 ) ) ;
#3003=ORIENTED_EDGE ( 'NONE', *, *, #2697, .T. ) ;
#3089=PLANE ( 'NONE',  #10432 ) ;
#3092=CARTESIAN_POINT ( 'NONE',  ( 5.000000000000000888, 0.000000000000000000, 0.000000000000000000 ) ) ;
#3122=PRODUCT_DEFINITION_FORMATION_WITH_SPECIFIED_SOURCE ( 'ANY', '', #12531, .NOT_KNOWN. ) ;
#3125=VERTEX_POINT ( 'NONE', #14156 ) ;
#3197=DIRECTION ( 'NONE',  ( 0.000000000000000000, -0.5000000000000013323, -0.8660254037844380415 ) ) ;
#3198=ORIENTED_EDGE ( 'NONE', *, *, #11207, .F. ) ;
#3238=VECTOR ( 'NONE', #5953, 1000.000000000000114 ) ;
#3272=VECTOR ( 'NONE', #10474, 1000.000000000000000 ) ;
#3279=DIRECTION ( 'NONE',  ( -1.000000000000000000, -0.000000000000000000, -0.000000000000000000 ) ) ;
#3281=CIRCLE ( 'NONE', #8216, 2.055000000000000160 ) ;
#3283=LINE ( 'NONE', #11108, #158 ) ;
#3319=AXIS2_PLACEMENT_3D ( 'NONE', #598, #2974, #14202 ) ;
#3324=CARTESIAN_POINT ( 'NONE',  ( 0.2500000000000002220, 5.204748896376250699E-16, -4.250000000000000000 ) ) ;
#3328=CARTESIAN_POINT ( 'NONE',  ( 2.500000000000000000, -1.178949249685214307, 2.042000000000001592 ) ) ;
#3397=CARTESIAN_POINT ( 'NONE',  ( 20.55500000000001748, 0.000000000000000000, 2.500000000000000888 ) ) ;
#3505=VECTOR ( 'NONE', #3197, 999.9999999999997726 ) ;
#3539=DIRECTION ( 'NONE',  ( 0.000000000000000000, 1.224646799147353207E-16, 1.000000000000000000 ) ) ;
#3543=DIRECTION ( 'NONE',  ( 0.000000000000000000, 0.000000000000000000, 1.000000000000000000 ) ) ;
#3564=AXIS2_PLACEMENT_3D ( 'NONE', #5747, #11485, #10244 ) ;
#3571=ORIENTED_EDGE ( 'NONE', *, *, #14350, .T. ) ;
#3590=APPLICATION_CONTEXT ( 'automotive_design' ) ;
#3635=EDGE_CURVE ( 'NONE', #8892, #12461, #4301, .T. ) ;
#3676=ADVANCED_FACE ( 'NONE', ( #12392 ), #10198, .F. ) ;
#3689=CARTESIAN_POINT ( 'NONE',  ( 2.500000000000000000, 1.178949249685212974, -2.042000000000001148 ) ) ;
#3699=DIRECTION ( 'NONE',  ( -0.7071067811865364705, 0.000000000000000000, 0.7071067811865584529 ) ) ;
#3701=ADVANCED_FACE ( 'NONE', ( #13880 ), #12844, .F. ) ;
#3729=( NAMED_UNIT ( * ) SI_UNIT ( $, .STERADIAN. ) SOLID_ANGLE_UNIT ( ) );
#3759=AXIS2_PLACEMENT_3D ( 'NONE', #2791, #12907, #7294 ) ;
#3771=EDGE_CURVE ( 'NONE', #9802, #7658, #9415, .T. ) ;
#3779=CIRCLE ( 'NONE', #12009, 2.041999999999999815 ) ;
#3791=CARTESIAN_POINT ( 'NONE',  ( 2.500000000000000000, 1.178949249685212974, -2.042000000000001148 ) ) ;
#3798=CARTESIAN_POINT ( 'NONE',  ( 0.000000000000000000, 2.357898499370431722, -2.818925648462311528E-15 ) ) ;
#3816=ORIENTED_EDGE ( 'NONE', *, *, #12956, .F. ) ;
#3841=CARTESIAN_POINT ( 'NONE',  ( 4.999999999999997335, 0.000000000000000000, 0.000000000000000000 ) ) ;
#3862=DIRECTION ( 'NONE',  ( 0.000000000000000000, 0.000000000000000000, 1.000000000000000000 ) ) ;
#3881=CARTESIAN_POINT ( 'NONE',  ( 2.500000000000000000, -2.357898499370432166, 3.035766082959412415E-15 ) ) ;
#3883=( LENGTH_UNIT ( ) NAMED_UNIT ( * ) SI_UNIT ( .MILLI., .METRE. ) );
#3914=DIRECTION ( 'NONE',  ( 0.000000000000000000, 0.000000000000000000, -1.000000000000000000 ) ) ;
#3981=ORIENTED_EDGE ( 'NONE', *, *, #5742, .F. ) ;
#3985=ORIENTED_EDGE ( 'NONE', *, *, #10710, .F. ) ;
#3995=ORIENTED_EDGE ( 'NONE', *, *, #518, .F. ) ;
#4008=EDGE_CURVE ( 'NONE', #5188, #7721, #5888, .T. ) ;
#4064=( NAMED_UNIT ( * ) SI_UNIT ( $, .STERADIAN. ) SOLID_ANGLE_UNIT ( ) );
#4071=CIRCLE ( 'NONE', #5950, 4.250000000000000000 ) ;
#4079=CYLINDRICAL_SURFACE ( 'NONE', #14588, 4.250000000000000000 ) ;
#4145=DIRECTION ( 'NONE',  ( 0.000000000000000000, -1.000000000000000000, 1.287488025362403787E-15 ) ) ;
#4160=DIRECTION ( 'NONE',  ( 0.000000000000000000, 0.000000000000000000, 1.000000000000000000 ) ) ;
#4166=VERTEX_POINT ( 'NONE', #13564 ) ;
#4172=DIRECTION ( 'NONE',  ( 1.000000000000000000, 0.000000000000000000, 0.000000000000000000 ) ) ;
#4187=FACE_OUTER_BOUND ( 'NONE', #464, .T. ) ;
#4193=CARTESIAN_POINT ( 'NONE',  ( 20.55500000000001748, 3.061616997868384127E-16, -2.500000000000000888 ) ) ;
#4230=ORIENTED_EDGE ( 'NONE', *, *, #14561, .T. ) ;
#4235=CARTESIAN_POINT ( 'NONE',  ( 2.500000000000000000, 2.357898499370431722, -2.818925648462311528E-15 ) ) ;
#4246=VERTEX_POINT ( 'NONE', #10909 ) ;
#4274=EDGE_LOOP ( 'NONE', ( #7569, #11902, #13356, #7417 ) ) ;
#4276=EDGE_CURVE ( 'NONE', #11781, #11591, #13439, .T. ) ;
#4280=VERTEX_POINT ( 'NONE', #10829 ) ;
#4301=LINE ( 'NONE', #12466, #13187 ) ;
#4347=CARTESIAN_POINT ( 'NONE',  ( 0.000000000000000000, 0.000000000000000000, 0.000000000000000000 ) ) ;
#4366=PLANE ( 'NONE',  #221 ) ;
#4386=ORIENTED_EDGE ( 'NONE', *, *, #14350, .F. ) ;
#4388=DIRECTION ( 'NONE',  ( 0.000000000000000000, 0.000000000000000000, 1.000000000000000000 ) ) ;
#4415=EDGE_LOOP ( 'NONE', ( #3985, #2706, #4386, #9688 ) ) ;
#4434=ORIENTED_EDGE ( 'NONE', *, *, #1395, .F. ) ;
#4456=AXIS2_PLACEMENT_3D ( 'NONE', #271, #13647, #3543 ) ;
#4467=ORIENTED_EDGE ( 'NONE', *, *, #6837, .T. ) ;
#4469=ORIENTED_EDGE ( 'NONE', *, *, #9319, .F. ) ;
#4542=EDGE_LOOP ( 'NONE', ( #13166, #13165, #13082 ) ) ;
#4560=ADVANCED_FACE ( 'NONE', ( #11468 ), #11548, .T. ) ;
#4590=EDGE_CURVE ( 'NONE', #783, #12163, #12733, .T. ) ;
#4598=UNCERTAINTY_MEASURE_WITH_UNIT (LENGTH_MEASURE( 1.000000000000000082E-05 ), #14243, 'distance_accuracy_value', 'NONE');
#4607=EDGE_CURVE ( 'NONE', #3125, #10404, #4784, .T. ) ;
#4609=VERTEX_POINT ( 'NONE', #1224 ) ;
#4629=ORIENTED_EDGE ( 'NONE', *, *, #14209, .T. ) ;
#4639=EDGE_CURVE ( 'NONE', #9573, #4953, #9206, .T. ) ;
#4640=ORIENTED_EDGE ( 'NONE', *, *, #1413, .F. ) ;
#4666=CARTESIAN_POINT ( 'NONE',  ( 2.500000000000000000, -2.357898499370432166, 3.035766082959412415E-15 ) ) ;
#4676=ORIENTED_EDGE ( 'NONE', *, *, #4639, .F. ) ;
#4699=ORIENTED_EDGE ( 'NONE', *, *, #13587, .F. ) ;
#4703=DIRECTION ( 'NONE',  ( 0.000000000000000000, 0.000000000000000000, 1.000000000000000000 ) ) ;
#4704=CARTESIAN_POINT ( 'NONE',  ( 0.000000000000000000, -1.178949249685214307, 2.042000000000001592 ) ) ;
#4750=CARTESIAN_POINT ( 'NONE',  ( 2.500000000000000000, 2.357898499370431722, -2.818925648462311528E-15 ) ) ;
#4760=ORIENTED_EDGE ( 'NONE', *, *, #6017, .T. ) ;
#4784=LINE ( 'NONE', #9341, #14165 ) ;
#4818=CARTESIAN_POINT ( 'NONE',  ( 2.500000000000000000, 2.357898499370431722, -2.818925648462311528E-15 ) ) ;
#4840=( LENGTH_UNIT ( ) NAMED_UNIT ( * ) SI_UNIT ( .MILLI., .METRE. ) );
#4862=AXIS2_PLACEMENT_3D ( 'NONE', #4887, #351, #13811 ) ;
#4883=CARTESIAN_POINT ( 'NONE',  ( 4.999999999999997335, 5.204748896376250699E-16, -4.250000000000000000 ) ) ;
#4887=CARTESIAN_POINT ( 'NONE',  ( 0.2500000000000002220, 0.000000000000000000, 0.000000000000000000 ) ) ;
#4900=MECHANICAL_DESIGN_GEOMETRIC_PRESENTATION_REPRESENTATION('',(#1105),#13143);
#4906=LINE ( 'NONE', #13905, #4962 ) ;
#4919=DIRECTION ( 'NONE',  ( -1.000000000000000000, -0.000000000000000000, -0.000000000000000000 ) ) ;
#4932=EDGE_CURVE ( 'NONE', #809, #5257, #2610, .T. ) ;
#4943=CARTESIAN_POINT ( 'NONE',  ( 2.500000000000000000, -2.357898499370432166, 3.035766082959412415E-15 ) ) ;
#4953=VERTEX_POINT ( 'NONE', #1875 ) ;
#4959=DIRECTION ( 'NONE',  ( 1.000000000000000000, 0.000000000000000000, 0.000000000000000000 ) ) ;
#4962=VECTOR ( 'NONE', #10576, 1000.000000000000000 ) ;
#4966=TOROIDAL_SURFACE ( 'NONE', #13207, 4.000000000000000000, 0.2500000000000000000 ) ;
#4970=AXIS2_PLACEMENT_3D ( 'NONE', #5794, #5728, #7044 ) ;
#4979=PLANE ( 'NONE',  #8473 ) ;
#5032=AXIS2_PLACEMENT_3D ( 'NONE', #11847, #8449, #9422 ) ;
#5038=FACE_OUTER_BOUND ( 'NONE', #12256, .T. ) ;
#5065=SURFACE_STYLE_FILL_AREA ( #10505 ) ;
#5086=ORIENTED_EDGE ( 'NONE', *, *, #11506, .F. ) ;
#5121=DIRECTION ( 'NONE',  ( -1.000000000000000000, -0.000000000000000000, -0.000000000000000000 ) ) ;
#5166=CARTESIAN_POINT ( 'NONE',  ( 2.500000000000000000, -1.178949249685214307, 2.042000000000001592 ) ) ;
#5188=VERTEX_POINT ( 'NONE', #7743 ) ;
#5191=DIRECTION ( 'NONE',  ( -1.000000000000000000, -0.000000000000000000, -0.000000000000000000 ) ) ;
#5201=ORIENTED_EDGE ( 'NONE', *, *, #14136, .T. ) ;
#5206=EDGE_CURVE ( 'NONE', #12163, #1716, #2199, .T. ) ;
#5213=AXIS2_PLACEMENT_3D ( 'NONE', #4750, #5766, #2506 ) ;
#5221=DIRECTION ( 'NONE',  ( -1.000000000000000000, -0.000000000000000000, -0.000000000000000000 ) ) ;
#5252=AXIS2_PLACEMENT_3D ( 'NONE', #6928, #2346, #3539 ) ;
#5257=VERTEX_POINT ( 'NONE', #13503 ) ;
#5324=DIRECTION ( 'NONE',  ( -1.000000000000000000, -0.000000000000000000, -0.000000000000000000 ) ) ;
#5338=CARTESIAN_POINT ( 'NONE',  ( 5.200000000000002842, 0.000000000000000000, -2.700000000000000622 ) ) ;
#5373=ADVANCED_FACE ( 'NONE', ( #5810 ), #8319, .T. ) ;
#5451=DIRECTION ( 'NONE',  ( 0.000000000000000000, -1.000000000000000000, 1.287488025362403787E-15 ) ) ;
#5503=ORIENTED_EDGE ( 'NONE', *, *, #5742, .T. ) ;
#5559=ADVANCED_FACE ( 'NONE', ( #4187 ), #8045, .F. ) ;
#5568=EDGE_LOOP ( 'NONE', ( #2377, #9073 ) ) ;
#5573=FACE_OUTER_BOUND ( 'NONE', #2944, .T. ) ;
#5597=EDGE_CURVE ( 'NONE', #10404, #4280, #6696, .T. ) ;
#5601=CARTESIAN_POINT ( 'NONE',  ( 3.678949249685231848, 0.000000000000000000, 0.000000000000000000 ) ) ;
#5606=FACE_OUTER_BOUND ( 'NONE', #11671, .T. ) ;
#5607=AXIS2_PLACEMENT_3D ( 'NONE', #8210, #11611, #10 ) ;
#5622=DIRECTION ( 'NONE',  ( 0.000000000000000000, 0.000000000000000000, -1.000000000000000000 ) ) ;
#5638=PLANE ( 'NONE',  #1599 ) ;
#5652=DIRECTION ( 'NONE',  ( -0.5000000000000051070, 0.000000000000000000, 0.8660254037844355990 ) ) ;
#5728=DIRECTION ( 'NONE',  ( 0.000000000000000000, -1.000000000000000000, 0.000000000000000000 ) ) ;
#5742=EDGE_CURVE ( 'NONE', #11030, #4280, #8145, .T. ) ;
#5747=CARTESIAN_POINT ( 'NONE',  ( 2.500000000000000000, 2.357898499370431722, -2.818925648462311528E-15 ) ) ;
#5756=ORIENTED_EDGE ( 'NONE', *, *, #10016, .T. ) ;
#5757=EDGE_CURVE ( 'NONE', #11781, #2369, #13838, .T. ) ;
#5766=DIRECTION ( 'NONE',  ( 1.000000000000000000, 0.000000000000000000, 0.000000000000000000 ) ) ;
#5782=FACE_OUTER_BOUND ( 'NONE', #825, .T. ) ;
#5794=CARTESIAN_POINT ( 'NONE',  ( 0.2500000000000002220, 0.000000000000000000, 4.000000000000000000 ) ) ;
#5810=FACE_OUTER_BOUND ( 'NONE', #14403, .T. ) ;
#5834=EDGE_CURVE ( 'NONE', #9095, #1716, #9196, .T. ) ;
#5835=AXIS2_PLACEMENT_3D ( 'NONE', #8448, #8230, #12741 ) ;
#5849=EDGE_LOOP ( 'NONE', ( #6138, #1298, #4760, #758 ) ) ;
#5855=SHAPE_REPRESENTATION_RELATIONSHIP ( 'NONE' , 'NONE' ,  #12910, #10030 ) ;
#5865=EDGE_CURVE ( 'NONE', #8019, #10404, #11407, .T. ) ;
#5868=CARTESIAN_POINT ( 'NONE',  ( 2.500000000000000000, -1.178949249685218748, -2.041999999999998039 ) ) ;
#5875=ORIENTED_EDGE ( 'NONE', *, *, #14481, .F. ) ;
#5880=AXIS2_PLACEMENT_3D ( 'NONE', #2324, #1007, #10015 ) ;
#5888=CIRCLE ( 'NONE', #9899, 2.041999999999999815 ) ;
#5906=LINE ( 'NONE', #5981, #9197 ) ;
#5916=AXIS2_PLACEMENT_3D ( 'NONE', #14434, #12126, #2987 ) ;
#5950=AXIS2_PLACEMENT_3D ( 'NONE', #3841, #1753, #7438 ) ;
#5953=DIRECTION ( 'NONE',  ( 0.000000000000000000, -0.5000000000000009992, -0.8660254037844380415 ) ) ;
#5981=CARTESIAN_POINT ( 'NONE',  ( 21.00000000000000355, 0.000000000000000000, 2.055000000000000160 ) ) ;
#6010=ORIENTED_EDGE ( 'NONE', *, *, #13587, .T. ) ;
#6017=EDGE_CURVE ( 'NONE', #7658, #9573, #1662, .T. ) ;
#6078=FACE_OUTER_BOUND ( 'NONE', #9353, .T. ) ;
#6083=EDGE_LOOP ( 'NONE', ( #6010, #14058, #10563, #5875 ) ) ;
#6087=VECTOR ( 'NONE', #5121, 1000.000000000000000 ) ;
#6096=VECTOR ( 'NONE', #12046, 1000.000000000000114 ) ;
#6138=ORIENTED_EDGE ( 'NONE', *, *, #8274, .F. ) ;
#6162=CIRCLE ( 'NONE', #7816, 2.500000000000000444 ) ;
#6169=VECTOR ( 'NONE', #13268, 1000.000000000000114 ) ;
#6197=ORIENTED_EDGE ( 'NONE', *, *, #3635, .F. ) ;
#6214=CARTESIAN_POINT ( 'NONE',  ( -31.74999999999995737, 0.000000000000000000, 0.000000000000000000 ) ) ;
#6218=ORIENTED_EDGE ( 'NONE', *, *, #12129, .T. ) ;
#6241=ORIENTED_EDGE ( 'NONE', *, *, #6017, .F. ) ;
#6245=FACE_OUTER_BOUND ( 'NONE', #5568, .T. ) ;
#6322=ADVANCED_FACE ( 'NONE', ( #1670 ), #13782, .F. ) ;
#6336=( NAMED_UNIT ( * ) PLANE_ANGLE_UNIT ( ) SI_UNIT ( $, .RADIAN. ) );
#6373=AXIS2_PLACEMENT_3D ( 'NONE', #8882, #3279, #12195 ) ;
#6380=CARTESIAN_POINT ( 'NONE',  ( 0.2500000000000002220, 0.000000000000000000, 0.000000000000000000 ) ) ;
#6417=DIRECTION ( 'NONE',  ( 1.000000000000000000, 0.000000000000000000, 0.000000000000000000 ) ) ;
#6418=AXIS2_PLACEMENT_3D ( 'NONE', #10741, #4172, #612 ) ;
#6423=( GEOMETRIC_REPRESENTATION_CONTEXT ( 3 ) GLOBAL_UNCERTAINTY_ASSIGNED_CONTEXT ( ( #7388 ) ) GLOBAL_UNIT_ASSIGNED_CONTEXT ( ( #3883, #1651, #10664 ) ) REPRESENTATION_CONTEXT ( 'NONE', 'WORKASPACE' ) );
#6456=DIRECTION ( 'NONE',  ( 0.000000000000000000, 0.000000000000000000, -1.000000000000000000 ) ) ;
#6467=ORIENTED_EDGE ( 'NONE', *, *, #8265, .T. ) ;
#6505=LINE ( 'NONE', #874, #12502 ) ;
#6517=ORIENTED_EDGE ( 'NONE', *, *, #12519, .F. ) ;
#6529=ORIENTED_EDGE ( 'NONE', *, *, #12956, .T. ) ;
#6541=CONICAL_SURFACE ( 'NONE', #13874, 2.055000000000000160, 0.7853981633974639331 ) ;
#6554=EDGE_CURVE ( 'NONE', #8892, #9095, #3283, .T. ) ;
#6558=ORIENTED_EDGE ( 'NONE', *, *, #12519, .T. ) ;
#6572=CARTESIAN_POINT ( 'NONE',  ( -31.74999999999995737, 0.000000000000000000, 0.000000000000000000 ) ) ;
#6637=PRODUCT_DEFINITION_SHAPE ( 'NONE', 'NONE',  #972 ) ;
#6696=LINE ( 'NONE', #11190, #6169 ) ;
#6711=CARTESIAN_POINT ( 'NONE',  ( 21.00000000000000355, 0.000000000000000000, 2.055000000000000160 ) ) ;
#6719=ORIENTED_EDGE ( 'NONE', *, *, #1906, .T. ) ;
#6722=DIRECTION ( 'NONE',  ( -1.000000000000000000, -0.000000000000000000, -0.000000000000000000 ) ) ;
#6724=ORIENTED_EDGE ( 'NONE', *, *, #9785, .F. ) ;
#6728=DIRECTION ( 'NONE',  ( 0.000000000000000000, 0.000000000000000000, 1.000000000000000000 ) ) ;
#6729=CARTESIAN_POINT ( 'NONE',  ( 2.500000000000000000, 2.357898499370431722, -2.818925648462311528E-15 ) ) ;
#6751=ADVANCED_FACE ( 'NONE', ( #6078 ), #13994, .T. ) ;
#6793=DIRECTION ( 'NONE',  ( 0.000000000000000000, 0.4999999999999990008, -0.8660254037844391517 ) ) ;
#6828=ORIENTED_EDGE ( 'NONE', *, *, #1270, .T. ) ;
#6837=EDGE_CURVE ( 'NONE', #2369, #1573, #182, .T. ) ;
#6856=LINE ( 'NONE', #1317, #10138 ) ;
#6861=FACE_OUTER_BOUND ( 'NONE', #6083, .T. ) ;
#6864=VECTOR ( 'NONE', #7938, 1000.000000000000000 ) ;
#6875=STYLED_ITEM ( 'NONE', ( #460 ), #10030 ) ;
#6908=DIRECTION ( 'NONE',  ( -1.000000000000000000, -0.000000000000000000, -0.000000000000000000 ) ) ;
#6928=CARTESIAN_POINT ( 'NONE',  ( 5.200000000000002842, 3.306546357697854226E-16, 2.700000000000000622 ) ) ;
#6936=ORIENTED_EDGE ( 'NONE', *, *, #1320, .F. ) ;
#6964=FACE_OUTER_BOUND ( 'NONE', #891, .T. ) ;
#6982=ORIENTED_EDGE ( 'NONE', *, *, #12467, .F. ) ;
#7000=VERTEX_POINT ( 'NONE', #973 ) ;
#7009=LINE ( 'NONE', #4666, #8978 ) ;
#7019=ADVANCED_FACE ( 'NONE', ( #8171 ), #11742, .T. ) ;
#7023=DIRECTION ( 'NONE',  ( 0.000000000000000000, -0.5000000000000013323, -0.8660254037844380415 ) ) ;
#7029=ORIENTED_EDGE ( 'NONE', *, *, #11207, .T. ) ;
#7044=DIRECTION ( 'NONE',  ( 0.000000000000000000, 0.000000000000000000, -1.000000000000000000 ) ) ;
#7059=ADVANCED_FACE ( 'NONE', ( #190 ), #10588, .T. ) ;
#7129=CARTESIAN_POINT ( 'NONE',  ( -31.74999999999995737, 3.061616997868383634E-16, -2.500000000000000444 ) ) ;
#7166=EDGE_CURVE ( 'NONE', #4609, #1573, #8466, .T. ) ;
#7241=VECTOR ( 'NONE', #8084, 1000.000000000000000 ) ;
#7249=AXIS2_PLACEMENT_3D ( 'NONE', #9367, #2878, #1609 ) ;
#7255=CARTESIAN_POINT ( 'NONE',  ( 2.500000000000000000, -1.178949249685214307, 2.042000000000001592 ) ) ;
#7287=AXIS2_PLACEMENT_3D ( 'NONE', #3092, #1980, #10979 ) ;
#7294=DIRECTION ( 'NONE',  ( 0.000000000000000000, 0.000000000000000000, 1.000000000000000000 ) ) ;
#7298=ORIENTED_EDGE ( 'NONE', *, *, #1976, .T. ) ;
#7303=AXIS2_PLACEMENT_3D ( 'NONE', #14016, #8387, #14078 ) ;
#7312=CARTESIAN_POINT ( 'NONE',  ( 0.000000000000000000, -1.178949249685214307, 2.042000000000001592 ) ) ;
#7323=CARTESIAN_POINT ( 'NONE',  ( 21.00000000000000355, 0.000000000000000000, 0.000000000000000000 ) ) ;
#7352=MECHANICAL_DESIGN_GEOMETRIC_PRESENTATION_REPRESENTATION('',(#6875),#6423);
#7388=UNCERTAINTY_MEASURE_WITH_UNIT (LENGTH_MEASURE( 1.000000000000000082E-05 ), #3883, 'distance_accuracy_value', 'NONE');
#7417=ORIENTED_EDGE ( 'NONE', *, *, #4276, .F. ) ;
#7421=DIRECTION ( 'NONE',  ( 0.000000000000000000, 0.000000000000000000, -1.000000000000000000 ) ) ;
#7438=DIRECTION ( 'NONE',  ( 0.000000000000000000, 0.000000000000000000, 1.000000000000000000 ) ) ;
#7445=CARTESIAN_POINT ( 'NONE',  ( 2.500000000000000000, 0.000000000000000000, 0.000000000000000000 ) ) ;
#7455=DIRECTION ( 'NONE',  ( 0.000000000000000000, 1.000000000000000000, -1.287488025362403787E-15 ) ) ;
#7474=LINE ( 'NONE', #7255, #1118 ) ;
#7554=CARTESIAN_POINT ( 'NONE',  ( 5.200000000000002842, 0.000000000000000000, 0.000000000000000000 ) ) ;
#7559=FACE_OUTER_BOUND ( 'NONE', #569, .T. ) ;
#7569=ORIENTED_EDGE ( 'NONE', *, *, #14433, .F. ) ;
#7630=CLOSED_SHELL ( 'NONE', ( #5559, #7829, #1191, #1636, #13066, #12893, #14164, #4560, #12019, #10204, #7019, #8664, #11170, #7059, #5373, #11867, #13319, #6751, #1151, #3676, #6322, #12681, #8395, #9992, #2381, #3701, #13964 ) ) ;
#7632=ORIENTED_EDGE ( 'NONE', *, *, #2697, .F. ) ;
#7658=VERTEX_POINT ( 'NONE', #1571 ) ;
#7669=ORIENTED_EDGE ( 'NONE', *, *, #4932, .F. ) ;
#7682=DIRECTION ( 'NONE',  ( -0.5000000000000051070, 1.060575238724903217E-16, -0.8660254037844355990 ) ) ;
#7720=CIRCLE ( 'NONE', #7249, 4.000000000000000000 ) ;
#7721=VERTEX_POINT ( 'NONE', #10446 ) ;
#7743=CARTESIAN_POINT ( 'NONE',  ( 2.500000000000000000, -2.629050547790028551E-15, -2.041999999999999815 ) ) ;
#7784=AXIS2_PLACEMENT_3D ( 'NONE', #1644, #9329, #2461 ) ;
#7787=DIRECTION ( 'NONE',  ( -1.000000000000000000, -0.000000000000000000, -0.000000000000000000 ) ) ;
#7816=AXIS2_PLACEMENT_3D ( 'NONE', #14238, #10014, #11043 ) ;
#7829=ADVANCED_FACE ( 'NONE', ( #7559 ), #4966, .T. ) ;
#7852=CARTESIAN_POINT ( 'NONE',  ( 5.000000000000002665, 0.000000000000000000, -2.700000000000000622 ) ) ;
#7929=FACE_OUTER_BOUND ( 'NONE', #4415, .T. ) ;
#7938=DIRECTION ( 'NONE',  ( -1.000000000000000000, -0.000000000000000000, -0.000000000000000000 ) ) ;
#7977=DIRECTION ( 'NONE',  ( -1.000000000000000000, -0.000000000000000000, -0.000000000000000000 ) ) ;
#8000=EDGE_CURVE ( 'NONE', #9573, #809, #2367, .T. ) ;
#8019=VERTEX_POINT ( 'NONE', #7312 ) ;
#8045=CONICAL_SURFACE ( 'NONE', #1, 2.041999999999999815, 1.047197551196591858 ) ;
#8061=ORIENTED_EDGE ( 'NONE', *, *, #1395, .T. ) ;
#8072=PLANE ( 'NONE',  #7784 ) ;
#8084=DIRECTION ( 'NONE',  ( 0.000000000000000000, -0.4999999999999993339, 0.8660254037844390407 ) ) ;
#8096=VERTEX_POINT ( 'NONE', #3791 ) ;
#8106=LINE ( 'NONE', #1088, #225 ) ;
#8145=LINE ( 'NONE', #5868, #10640 ) ;
#8158=ORIENTED_EDGE ( 'NONE', *, *, #4607, .T. ) ;
#8171=FACE_OUTER_BOUND ( 'NONE', #4274, .T. ) ;
#8210=CARTESIAN_POINT ( 'NONE',  ( 5.200000000000002842, 0.000000000000000000, 0.000000000000000000 ) ) ;
#8216=AXIS2_PLACEMENT_3D ( 'NONE', #7323, #14116, #1853 ) ;
#8230=DIRECTION ( 'NONE',  ( 1.000000000000000000, 0.000000000000000000, 0.000000000000000000 ) ) ;
#8265=EDGE_CURVE ( 'NONE', #1716, #4246, #806, .T. ) ;
#8274=EDGE_CURVE ( 'NONE', #9802, #809, #6505, .T. ) ;
#8319=PLANE ( 'NONE',  #3564 ) ;
#8324=LINE ( 'NONE', #3689, #3272 ) ;
#8360=CARTESIAN_POINT ( 'NONE',  ( 2.500000000000000000, 0.000000000000000000, 0.000000000000000000 ) ) ;
#8361=CARTESIAN_POINT ( 'NONE',  ( 5.200000000000002842, 0.000000000000000000, 2.500000000000000444 ) ) ;
#8362=DIRECTION ( 'NONE',  ( -0.000000000000000000, 0.8660254037844392627, 0.4999999999999990008 ) ) ;
#8387=DIRECTION ( 'NONE',  ( -1.000000000000000000, -0.000000000000000000, -0.000000000000000000 ) ) ;
#8395=ADVANCED_FACE ( 'NONE', ( #5606 ), #4366, .F. ) ;
#8440=CARTESIAN_POINT ( 'NONE',  ( 5.200000000000002842, 3.061616997868383634E-16, -2.500000000000000444 ) ) ;
#8448=CARTESIAN_POINT ( 'NONE',  ( 2.500000000000000000, 2.357898499370431722, -2.818925648462311528E-15 ) ) ;
#8449=DIRECTION ( 'NONE',  ( 1.000000000000000000, 0.000000000000000000, 0.000000000000000000 ) ) ;
#8466=CIRCLE ( 'NONE', #7287, 2.700000000000000622 ) ;
#8473=AXIS2_PLACEMENT_3D ( 'NONE', #13086, #12935, #2743 ) ;
#8486=CONICAL_SURFACE ( 'NONE', #6373, 2.041999999999999815, 1.047197551196591858 ) ;
#8493=CARTESIAN_POINT ( 'NONE',  ( 2.500000000000000000, 0.000000000000000000, 0.000000000000000000 ) ) ;
#8568=DIRECTION ( 'NONE',  ( -1.000000000000000000, -0.000000000000000000, -0.000000000000000000 ) ) ;
#8572=DIRECTION ( 'NONE',  ( 0.000000000000000000, 0.000000000000000000, 1.000000000000000000 ) ) ;
#8651=EDGE_LOOP ( 'NONE', ( #12169, #6936, #12926, #6828, #8158 ) ) ;
#8664=ADVANCED_FACE ( 'NONE', ( #5573 ), #11034, .T. ) ;
#8681=DIRECTION ( 'NONE',  ( 1.000000000000000000, 0.000000000000000000, 0.000000000000000000 ) ) ;
#8734=CARTESIAN_POINT ( 'NONE',  ( 0.000000000000000000, 0.000000000000000000, 0.000000000000000000 ) ) ;
#8795=DIRECTION ( 'NONE',  ( -1.000000000000000000, -0.000000000000000000, -0.000000000000000000 ) ) ;
#8800=DIRECTION ( 'NONE',  ( 0.000000000000000000, 0.8660254037844380415, -0.5000000000000012212 ) ) ;
#8839=DIRECTION ( 'NONE',  ( 0.000000000000000000, -0.4999999999999993339, 0.8660254037844390407 ) ) ;
#8849=CARTESIAN_POINT ( 'NONE',  ( 0.000000000000000000, -2.357898499370432166, 3.035766082959412415E-15 ) ) ;
#8854=APPLICATION_CONTEXT ( 'automotive_design' ) ;
#8861=ORIENTED_EDGE ( 'NONE', *, *, #5834, .T. ) ;
#8882=CARTESIAN_POINT ( 'NONE',  ( 2.500000000000000000, 0.000000000000000000, 0.000000000000000000 ) ) ;
#8892=VERTEX_POINT ( 'NONE', #12949 ) ;
#8978=VECTOR ( 'NONE', #6793, 1000.000000000000114 ) ;
#9011=DIRECTION ( 'NONE',  ( 1.000000000000000000, 0.000000000000000000, 0.000000000000000000 ) ) ;
#9017=DIRECTION ( 'NONE',  ( 0.000000000000000000, 0.5000000000000011102, 0.8660254037844379305 ) ) ;
#9040=DIRECTION ( 'NONE',  ( 0.000000000000000000, -0.4999999999999993339, 0.8660254037844390407 ) ) ;
#9053=CARTESIAN_POINT ( 'NONE',  ( 2.500000000000000000, 0.000000000000000000, 0.000000000000000000 ) ) ;
#9073=ORIENTED_EDGE ( 'NONE', *, *, #3771, .F. ) ;
#9095=VERTEX_POINT ( 'NONE', #14215 ) ;
#9137=DIRECTION ( 'NONE',  ( -0.7071067811865364705, 8.659560562355067211E-17, -0.7071067811865584529 ) ) ;
#9196=LINE ( 'NONE', #1517, #7241 ) ;
#9197=VECTOR ( 'NONE', #3699, 1000.000000000000114 ) ;
#9206=CIRCLE ( 'NONE', #4970, 0.2500000000000002220 ) ;
#9213=VECTOR ( 'NONE', #5324, 1000.000000000000000 ) ;
#9224=AXIS2_PLACEMENT_3D ( 'NONE', #9941, #8681, #3914 ) ;
#9319=EDGE_CURVE ( 'NONE', #12461, #1135, #445, .T. ) ;
#9326=CIRCLE ( 'NONE', #4862, 4.250000000000000000 ) ;
#9329=DIRECTION ( 'NONE',  ( -1.000000000000000000, 0.000000000000000000, -0.000000000000000000 ) ) ;
#9341=CARTESIAN_POINT ( 'NONE',  ( 2.500000000000000000, -2.357898499370432166, 3.035766082959412415E-15 ) ) ;
#9353=EDGE_LOOP ( 'NONE', ( #1886, #10669, #5756, #4230, #5503 ) ) ;
#9367=CARTESIAN_POINT ( 'NONE',  ( 0.000000000000000000, 0.000000000000000000, 0.000000000000000000 ) ) ;
#9401=DIRECTION ( 'NONE',  ( 0.000000000000000000, 0.000000000000000000, 1.000000000000000000 ) ) ;
#9405=( NAMED_UNIT ( * ) PLANE_ANGLE_UNIT ( ) SI_UNIT ( $, .RADIAN. ) );
#9409=ORIENTED_EDGE ( 'NONE', *, *, #2718, .T. ) ;
#9415=CIRCLE ( 'NONE', #14368, 4.250000000000000000 ) ;
#9422=DIRECTION ( 'NONE',  ( 0.000000000000000000, 0.000000000000000000, -1.000000000000000000 ) ) ;
#9440=AXIS2_PLACEMENT_3D ( 'NONE', #4347, #14302, #6417 ) ;
#9537=DIRECTION ( 'NONE',  ( -1.000000000000000000, -0.000000000000000000, -0.000000000000000000 ) ) ;
#9573=VERTEX_POINT ( 'NONE', #879 ) ;
#9597=PRODUCT_DEFINITION_CONTEXT ( 'detailed design', #8854, 'design' ) ;
#9628=ORIENTED_EDGE ( 'NONE', *, *, #4639, .T. ) ;
#9636=PLANE ( 'NONE',  #1829 ) ;
#9669=ORIENTED_EDGE ( 'NONE', *, *, #1760, .T. ) ;
#9685=VECTOR ( 'NONE', #5191, 1000.000000000000000 ) ;
#9688=ORIENTED_EDGE ( 'NONE', *, *, #6837, .F. ) ;
#9711=EDGE_LOOP ( 'NONE', ( #2655, #13860, #13498 ) ) ;
#9756=LINE ( 'NONE', #736, #1622 ) ;
#9785=EDGE_CURVE ( 'NONE', #14483, #11591, #5906, .T. ) ;
#9802=VERTEX_POINT ( 'NONE', #4883 ) ;
#9858=CIRCLE ( 'NONE', #408, 4.000000000000000000 ) ;
#9887=UNCERTAINTY_MEASURE_WITH_UNIT (LENGTH_MEASURE( 1.000000000000000082E-05 ), #4840, 'distance_accuracy_value', 'NONE');
#9891=CARTESIAN_POINT ( 'NONE',  ( 0.000000000000000000, -1.178949249685214307, 2.042000000000001592 ) ) ;
#9899=AXIS2_PLACEMENT_3D ( 'NONE', #12225, #1986, #14527 ) ;
#9941=CARTESIAN_POINT ( 'NONE',  ( 21.00000000000000000, 2.055000000000000160, 0.000000000000000000 ) ) ;
#9992=ADVANCED_FACE ( 'NONE', ( #1485 ), #10266, .F. ) ;
#9998=CARTESIAN_POINT ( 'NONE',  ( 2.500000000000000000, 0.000000000000000000, 0.000000000000000000 ) ) ;
#10014=DIRECTION ( 'NONE',  ( 1.000000000000000000, 0.000000000000000000, 0.000000000000000000 ) ) ;
#10015=DIRECTION ( 'NONE',  ( 0.000000000000000000, 0.000000000000000000, 1.000000000000000000 ) ) ;
#10016=EDGE_CURVE ( 'NONE', #3125, #7721, #7009, .T. ) ;
#10024=CARTESIAN_POINT ( 'NONE',  ( 2.500000000000000000, -1.178949249685214307, 2.042000000000001592 ) ) ;
#10030=ADVANCED_BREP_SHAPE_REPRESENTATION ( '', ( #2215, #9440 ), #2396 ) ;
#10036=EDGE_LOOP ( 'NONE', ( #3571, #1524 ) ) ;
#10095=AXIS2_PLACEMENT_3D ( 'NONE', #7445, #1617, #10631 ) ;
#10109=PRODUCT_CONTEXT ( 'NONE', #3590, 'mechanical' ) ;
#10110=DIRECTION ( 'NONE',  ( 0.000000000000000000, 0.000000000000000000, -1.000000000000000000 ) ) ;
#10114=AXIS2_PLACEMENT_3D ( 'NONE', #5338, #2003, #6456 ) ;
#10126=CARTESIAN_POINT ( 'NONE',  ( 0.2500000000000002220, 0.000000000000000000, 0.000000000000000000 ) ) ;
#10138=VECTOR ( 'NONE', #12677, 1000.000000000000000 ) ;
#10180=DIRECTION ( 'NONE',  ( 0.000000000000000000, 1.000000000000000000, -1.287488025362403787E-15 ) ) ;
#10198=PLANE ( 'NONE',  #1635 ) ;
#10204=ADVANCED_FACE ( 'NONE', ( #5038 ), #431, .T. ) ;
#10215=ORIENTED_EDGE ( 'NONE', *, *, #1320, .T. ) ;
#10217=ORIENTED_EDGE ( 'NONE', *, *, #4590, .T. ) ;
#10244=DIRECTION ( 'NONE',  ( 0.000000000000000000, 0.4999999999999992784, -0.8660254037844389297 ) ) ;
#10266=PLANE ( 'NONE',  #5213 ) ;
#10270=EDGE_CURVE ( 'NONE', #4166, #8096, #1018, .T. ) ;
#10283=ORIENTED_EDGE ( 'NONE', *, *, #1976, .F. ) ;
#10324=ORIENTED_EDGE ( 'NONE', *, *, #4276, .T. ) ;
#10332=DIRECTION ( 'NONE',  ( 0.000000000000000000, 0.000000000000000000, -1.000000000000000000 ) ) ;
#10361=CARTESIAN_POINT ( 'NONE',  ( 2.500000000000000000, 1.178949249685212974, -2.042000000000001148 ) ) ;
#10377=CARTESIAN_POINT ( 'NONE',  ( 2.500000000000000000, -1.178949249685218748, -2.041999999999998039 ) ) ;
#10404=VERTEX_POINT ( 'NONE', #8849 ) ;
#10416=DIRECTION ( 'NONE',  ( 0.000000000000000000, 0.000000000000000000, 1.000000000000000000 ) ) ;
#10432=AXIS2_PLACEMENT_3D ( 'NONE', #1977, #927, #5451 ) ;
#10440=DIRECTION ( 'NONE',  ( 0.000000000000000000, -1.287488025362403787E-15, -1.000000000000000000 ) ) ;
#10446=CARTESIAN_POINT ( 'NONE',  ( 2.500000000000000000, -1.768423874527825568, -1.020999999999998575 ) ) ;
#10474=DIRECTION ( 'NONE',  ( 0.000000000000000000, -1.000000000000000000, 1.287488025362403787E-15 ) ) ;
#10505=FILL_AREA_STYLE ('',( #1569 ) ) ;
#10538=DIRECTION ( 'NONE',  ( 0.000000000000000000, 0.4999999999999990008, -0.8660254037844391517 ) ) ;
#10547=DIRECTION ( 'NONE',  ( 0.000000000000000000, 1.000000000000000000, -1.287488025362403787E-15 ) ) ;
#10563=ORIENTED_EDGE ( 'NONE', *, *, #1413, .T. ) ;
#10576=DIRECTION ( 'NONE',  ( 0.000000000000000000, -1.000000000000000000, 1.287488025362403787E-15 ) ) ;
#10588=TOROIDAL_SURFACE ( 'NONE', #3759, 4.000000000000000000, 0.2500000000000000000 ) ;
#10617=AXIS2_PLACEMENT_3D ( 'NONE', #1139, #6908, #4703 ) ;
#10631=DIRECTION ( 'NONE',  ( 0.000000000000000000, 0.000000000000000000, 1.000000000000000000 ) ) ;
#10640=VECTOR ( 'NONE', #4919, 1000.000000000000000 ) ;
#10664=( NAMED_UNIT ( * ) SI_UNIT ( $, .STERADIAN. ) SOLID_ANGLE_UNIT ( ) );
#10669=ORIENTED_EDGE ( 'NONE', *, *, #4607, .F. ) ;
#10710=EDGE_CURVE ( 'NONE', #1324, #2369, #6162, .T. ) ;
#10741=CARTESIAN_POINT ( 'NONE',  ( 5.200000000000002842, 0.000000000000000000, 0.000000000000000000 ) ) ;
#10817=AXIS2_PLACEMENT_3D ( 'NONE', #6572, #11067, #949 ) ;
#10819=CARTESIAN_POINT ( 'NONE',  ( 2.500000000000000000, 2.629050547790028946E-15, 2.042000000000000259 ) ) ;
#10829=CARTESIAN_POINT ( 'NONE',  ( 0.000000000000000000, -1.178949249685218748, -2.041999999999998039 ) ) ;
#10909=CARTESIAN_POINT ( 'NONE',  ( 0.000000000000000000, 1.178949249685217415, 2.041999999999998483 ) ) ;
#10932=DIRECTION ( 'NONE',  ( -1.000000000000000000, -0.000000000000000000, -0.000000000000000000 ) ) ;
#10979=DIRECTION ( 'NONE',  ( 0.000000000000000000, 0.000000000000000000, -1.000000000000000000 ) ) ;
#10987=CARTESIAN_POINT ( 'NONE',  ( 2.500000000000000000, 2.357898499370431722, -2.818925648462311528E-15 ) ) ;
#11008=LINE ( 'NONE', #822, #6096 ) ;
#11030=VERTEX_POINT ( 'NONE', #10377 ) ;
#11034=PLANE ( 'NONE',  #9224 ) ;
#11043=DIRECTION ( 'NONE',  ( 0.000000000000000000, 0.000000000000000000, -1.000000000000000000 ) ) ;
#11067=DIRECTION ( 'NONE',  ( -1.000000000000000000, -0.000000000000000000, -0.000000000000000000 ) ) ;
#11087=DIRECTION ( 'NONE',  ( 1.000000000000000000, 0.000000000000000000, 0.000000000000000000 ) ) ;
#11108=CARTESIAN_POINT ( 'NONE',  ( 2.500000000000000000, 2.357898499370431722, -2.818925648462311528E-15 ) ) ;
#11170=ADVANCED_FACE ( 'NONE', ( #14142 ), #19, .F. ) ;
#11184=ORIENTED_EDGE ( 'NONE', *, *, #13484, .T. ) ;
#11190=CARTESIAN_POINT ( 'NONE',  ( 0.000000000000000000, -2.357898499370432166, 3.035766082959412415E-15 ) ) ;
#11207=EDGE_CURVE ( 'NONE', #12163, #9095, #1691, .T. ) ;
#11383=DIRECTION ( 'NONE',  ( 1.000000000000000000, 0.000000000000000000, 0.000000000000000000 ) ) ;
#11407=LINE ( 'NONE', #4704, #3238 ) ;
#11443=EDGE_LOOP ( 'NONE', ( #12975, #12413, #2249, #6517, #717 ) ) ;
#11450=DIRECTION ( 'NONE',  ( -1.000000000000000000, -0.000000000000000000, -0.000000000000000000 ) ) ;
#11468=FACE_OUTER_BOUND ( 'NONE', #5849, .T. ) ;
#11485=DIRECTION ( 'NONE',  ( 0.000000000000000000, -0.8660254037844390407, -0.4999999999999993339 ) ) ;
#11499=CIRCLE ( 'NONE', #10095, 2.041999999999999815 ) ;
#11506=EDGE_CURVE ( 'NONE', #1324, #4609, #12782, .T. ) ;
#11548=CYLINDRICAL_SURFACE ( 'NONE', #10617, 4.250000000000000000 ) ;
#11561=EDGE_LOOP ( 'NONE', ( #6529, #3981, #465, #11850, #11920 ) ) ;
#11579=EDGE_LOOP ( 'NONE', ( #7669, #12068, #9628, #4434 ) ) ;
#11591=VERTEX_POINT ( 'NONE', #3397 ) ;
#11610=FACE_BOUND ( 'NONE', #1795, .T. ) ;
#11611=DIRECTION ( 'NONE',  ( 1.000000000000000000, 0.000000000000000000, 0.000000000000000000 ) ) ;
#11620=EDGE_CURVE ( 'NONE', #7658, #9802, #4071, .T. ) ;
#11671=EDGE_LOOP ( 'NONE', ( #6982, #9409, #13611 ) ) ;
#11736=AXIS2_PLACEMENT_3D ( 'NONE', #8493, #9537, #3862 ) ;
#11742=CONICAL_SURFACE ( 'NONE', #4456, 2.055000000000000160, 0.7853981633974639331 ) ;
#11756=CARTESIAN_POINT ( 'NONE',  ( -31.74999999999995737, 0.000000000000000000, 4.250000000000000000 ) ) ;
#11781=VERTEX_POINT ( 'NONE', #4193 ) ;
#11813=FACE_OUTER_BOUND ( 'NONE', #193, .T. ) ;
#11847=CARTESIAN_POINT ( 'NONE',  ( 5.000000000000000888, 4.250000000000000000, 0.000000000000000000 ) ) ;
#11850=ORIENTED_EDGE ( 'NONE', *, *, #14209, .F. ) ;
#11867=ADVANCED_FACE ( 'NONE', ( #13121 ), #3089, .F. ) ;
#11902=ORIENTED_EDGE ( 'NONE', *, *, #13297, .T. ) ;
#11920=ORIENTED_EDGE ( 'NONE', *, *, #14317, .T. ) ;
#11961=TOROIDAL_SURFACE ( 'NONE', #5607, 2.700000000000000622, 0.2000000000000000111 ) ;
#12009=AXIS2_PLACEMENT_3D ( 'NONE', #8360, #12866, #9401 ) ;
#12019=ADVANCED_FACE ( 'NONE', ( #2772, #6245 ), #1671, .T. ) ;
#12046=DIRECTION ( 'NONE',  ( 0.000000000000000000, -0.5000000000000009992, -0.8660254037844380415 ) ) ;
#12068=ORIENTED_EDGE ( 'NONE', *, *, #8000, .F. ) ;
#12077=EDGE_LOOP ( 'NONE', ( #12892, #6558, #7632 ) ) ;
#12100=LINE ( 'NONE', #2052, #13170 ) ;
#12126=DIRECTION ( 'NONE',  ( -0.000000000000000000, 1.000000000000000000, 1.224646799147353207E-16 ) ) ;
#12129=EDGE_CURVE ( 'NONE', #14483, #7000, #12320, .T. ) ;
#12140=ORIENTED_EDGE ( 'NONE', *, *, #14136, .F. ) ;
#12163=VERTEX_POINT ( 'NONE', #10819 ) ;
#12164=LINE ( 'NONE', #9891, #2760 ) ;
#12169=ORIENTED_EDGE ( 'NONE', *, *, #5865, .F. ) ;
#12195=DIRECTION ( 'NONE',  ( 0.000000000000000000, 0.000000000000000000, 1.000000000000000000 ) ) ;
#12212=LINE ( 'NONE', #13272, #12957 ) ;
#12225=CARTESIAN_POINT ( 'NONE',  ( 2.500000000000000000, 0.000000000000000000, 0.000000000000000000 ) ) ;
#12256=EDGE_LOOP ( 'NONE', ( #969, #10324, #12882, #12748 ) ) ;
#12270=ORIENTED_EDGE ( 'NONE', *, *, #2718, .F. ) ;
#12275=VECTOR ( 'NONE', #7023, 999.9999999999997726 ) ;
#12320=CIRCLE ( 'NONE', #14224, 2.055000000000000160 ) ;
#12338=FACE_OUTER_BOUND ( 'NONE', #9711, .T. ) ;
#12392=FACE_OUTER_BOUND ( 'NONE', #11443, .T. ) ;
#12413=ORIENTED_EDGE ( 'NONE', *, *, #14317, .F. ) ;
#12436=AXIS2_PLACEMENT_3D ( 'NONE', #7554, #11087, #888 ) ;
#12445=VECTOR ( 'NONE', #10547, 1000.000000000000000 ) ;
#12461=VERTEX_POINT ( 'NONE', #13024 ) ;
#12466=CARTESIAN_POINT ( 'NONE',  ( 2.500000000000000000, 2.357898499370431722, -2.818925648462311528E-15 ) ) ;
#12467=EDGE_CURVE ( 'NONE', #13064, #14191, #11008, .T. ) ;
#12502=VECTOR ( 'NONE', #8795, 1000.000000000000000 ) ;
#12519=EDGE_CURVE ( 'NONE', #8892, #4166, #14341, .T. ) ;
#12531=PRODUCT ( 'socket head cap screw_iso_ISO 4762 M5 x 16 - 16N', 'socket head cap screw_iso_ISO 4762 M5 x 16 - 16N', '', ( #10109 ) ) ;
#12628=CARTESIAN_POINT ( 'NONE',  ( 2.500000000000000000, 1.178949249685217415, 2.041999999999998483 ) ) ;
#12641=DIRECTION ( 'NONE',  ( -1.000000000000000000, -0.000000000000000000, -0.000000000000000000 ) ) ;
#12651=DIRECTION ( 'NONE',  ( -1.000000000000000000, -0.000000000000000000, -0.000000000000000000 ) ) ;
#12664=AXIS2_PLACEMENT_3D ( 'NONE', #3881, #8362, #2750 ) ;
#12677=DIRECTION ( 'NONE',  ( -1.000000000000000000, -0.000000000000000000, -0.000000000000000000 ) ) ;
#12681=ADVANCED_FACE ( 'NONE', ( #12338 ), #2222, .F. ) ;
#12712=CIRCLE ( 'NONE', #5880, 2.500000000000000888 ) ;
#12733=LINE ( 'NONE', #312, #939 ) ;
#12741=DIRECTION ( 'NONE',  ( 0.000000000000000000, 0.000000000000000000, -1.000000000000000000 ) ) ;
#12746=VECTOR ( 'NONE', #10538, 1000.000000000000114 ) ;
#12748=ORIENTED_EDGE ( 'NONE', *, *, #10710, .T. ) ;
#12782=CIRCLE ( 'NONE', #5252, 0.2000000000000000944 ) ;
#12795=EDGE_LOOP ( 'NONE', ( #5086, #4640, #4467, #13682 ) ) ;
#12802=LINE ( 'NONE', #599, #6087 ) ;
#12844=PLANE ( 'NONE',  #14600 ) ;
#12866=DIRECTION ( 'NONE',  ( -1.000000000000000000, -0.000000000000000000, -0.000000000000000000 ) ) ;
#12882=ORIENTED_EDGE ( 'NONE', *, *, #14481, .T. ) ;
#12892=ORIENTED_EDGE ( 'NONE', *, *, #6554, .F. ) ;
#12893=ADVANCED_FACE ( 'NONE', ( #11813 ), #4079, .T. ) ;
#12907=DIRECTION ( 'NONE',  ( -1.000000000000000000, -0.000000000000000000, -0.000000000000000000 ) ) ;
#12910=SHAPE_REPRESENTATION ( 'socket head cap screw_iso_ISO 4762 M5 x 16 - 16N', ( #9440 ), #2396 ) ;
#12926=ORIENTED_EDGE ( 'NONE', *, *, #12467, .T. ) ;
#12935=DIRECTION ( 'NONE',  ( 0.000000000000000000, 0.8660254037844380415, -0.5000000000000009992 ) ) ;
#12939=LINE ( 'NONE', #14533, #9685 ) ;
#12949=CARTESIAN_POINT ( 'NONE',  ( 2.500000000000000000, 2.357898499370431722, -2.818925648462311528E-15 ) ) ;
#12956=EDGE_CURVE ( 'NONE', #1135, #4280, #9756, .T. ) ;
#12957=VECTOR ( 'NONE', #8839, 1000.000000000000000 ) ;
#12964=ORIENTED_EDGE ( 'NONE', *, *, #518, .T. ) ;
#12975=ORIENTED_EDGE ( 'NONE', *, *, #9319, .T. ) ;
#12982=LINE ( 'NONE', #4943, #12746 ) ;
#13005=CARTESIAN_POINT ( 'NONE',  ( 2.500000000000000000, 1.178949249685217415, 2.041999999999998483 ) ) ;
#13007=ORIENTED_EDGE ( 'NONE', *, *, #5834, .F. ) ;
#13014=FACE_OUTER_BOUND ( 'NONE', #8651, .T. ) ;
#13024=CARTESIAN_POINT ( 'NONE',  ( 0.000000000000000000, 2.357898499370431722, -2.818925648462311528E-15 ) ) ;
#13037=CARTESIAN_POINT ( 'NONE',  ( 2.500000000000000000, 2.357898499370431722, -2.818925648462311528E-15 ) ) ;
#13039=ORIENTED_EDGE ( 'NONE', *, *, #13297, .F. ) ;
#13064=VERTEX_POINT ( 'NONE', #3328 ) ;
#13066=ADVANCED_FACE ( 'NONE', ( #6861 ), #2053, .T. ) ;
#13068=LINE ( 'NONE', #5166, #12445 ) ;
#13082=ORIENTED_EDGE ( 'NONE', *, *, #4008, .F. ) ;
#13086=CARTESIAN_POINT ( 'NONE',  ( 2.500000000000000000, -1.178949249685214307, 2.042000000000001592 ) ) ;
#13097=DIRECTION ( 'NONE',  ( -1.000000000000000000, -0.000000000000000000, -0.000000000000000000 ) ) ;
#13121=FACE_OUTER_BOUND ( 'NONE', #14506, .T. ) ;
#13143=( GEOMETRIC_REPRESENTATION_CONTEXT ( 3 ) GLOBAL_UNCERTAINTY_ASSIGNED_CONTEXT ( ( #4598 ) ) GLOBAL_UNIT_ASSIGNED_CONTEXT ( ( #14243, #6336, #4064 ) ) REPRESENTATION_CONTEXT ( 'NONE', 'WORKASPACE' ) );
#13165=ORIENTED_EDGE ( 'NONE', *, *, #14561, .F. ) ;
#13166=ORIENTED_EDGE ( 'NONE', *, *, #873, .T. ) ;
#13170=VECTOR ( 'NONE', #7682, 1000.000000000000114 ) ;
#13187=VECTOR ( 'NONE', #6722, 1000.000000000000000 ) ;
#13207=AXIS2_PLACEMENT_3D ( 'NONE', #6380, #13097, #13244 ) ;
#13244=DIRECTION ( 'NONE',  ( 0.000000000000000000, 0.000000000000000000, 1.000000000000000000 ) ) ;
#13268=DIRECTION ( 'NONE',  ( 0.000000000000000000, 0.4999999999999990008, -0.8660254037844391517 ) ) ;
#13272=CARTESIAN_POINT ( 'NONE',  ( 0.000000000000000000, 2.357898499370431722, -2.818925648462311528E-15 ) ) ;
#13297=EDGE_CURVE ( 'NONE', #7000, #14483, #3281, .T. ) ;
#13319=ADVANCED_FACE ( 'NONE', ( #13014 ), #4979, .T. ) ;
#13342=ORIENTED_EDGE ( 'NONE', *, *, #2150, .T. ) ;
#13356=ORIENTED_EDGE ( 'NONE', *, *, #9785, .T. ) ;
#13439=CIRCLE ( 'NONE', #7303, 2.500000000000000888 ) ;
#13459=VECTOR ( 'NONE', #14253, 999.9999999999997726 ) ;
#13484=EDGE_CURVE ( 'NONE', #12461, #4246, #12212, .T. ) ;
#13498=ORIENTED_EDGE ( 'NONE', *, *, #14132, .F. ) ;
#13503=CARTESIAN_POINT ( 'NONE',  ( 0.000000000000000000, 5.051668046482832750E-16, -4.000000000000000000 ) ) ;
#13542=FACE_OUTER_BOUND ( 'NONE', #11561, .T. ) ;
#13550=ORIENTED_EDGE ( 'NONE', *, *, #4590, .F. ) ;
#13552=DIRECTION ( 'NONE',  ( 0.000000000000000000, 0.000000000000000000, 1.000000000000000000 ) ) ;
#13564=CARTESIAN_POINT ( 'NONE',  ( 2.500000000000000000, 1.768423874527822459, -1.021000000000002794 ) ) ;
#13587=EDGE_CURVE ( 'NONE', #11591, #11781, #12712, .T. ) ;
#13611=ORIENTED_EDGE ( 'NONE', *, *, #1760, .F. ) ;
#13631=ORIENTED_EDGE ( 'NONE', *, *, #6554, .T. ) ;
#13647=DIRECTION ( 'NONE',  ( -1.000000000000000000, -0.000000000000000000, -0.000000000000000000 ) ) ;
#13682=ORIENTED_EDGE ( 'NONE', *, *, #7166, .F. ) ;
#13720=COLOUR_RGB ( '',1.000000000000000000, 0.9490196078431372140, 0.9098039215686274384 ) ;
#13762=CARTESIAN_POINT ( 'NONE',  ( 2.500000000000000000, -1.768423874527823569, 1.021000000000002350 ) ) ;
#13782=PLANE ( 'NONE',  #5835 ) ;
#13811=DIRECTION ( 'NONE',  ( 0.000000000000000000, 0.000000000000000000, 1.000000000000000000 ) ) ;
#13838=LINE ( 'NONE', #7129, #6864 ) ;
#13860=ORIENTED_EDGE ( 'NONE', *, *, #1270, .F. ) ;
#13874=AXIS2_PLACEMENT_3D ( 'NONE', #2221, #7977, #6728 ) ;
#13880=FACE_OUTER_BOUND ( 'NONE', #14294, .T. ) ;
#13905=CARTESIAN_POINT ( 'NONE',  ( 2.500000000000000000, 1.178949249685212974, -2.042000000000001148 ) ) ;
#13912=SURFACE_STYLE_USAGE ( .BOTH. , #371 ) ;
#13937=ORIENTED_EDGE ( 'NONE', *, *, #13484, .F. ) ;
#13964=ADVANCED_FACE ( 'NONE', ( #5782 ), #8486, .F. ) ;
#13994=PLANE ( 'NONE',  #12664 ) ;
#14016=CARTESIAN_POINT ( 'NONE',  ( 20.55500000000001748, 0.000000000000000000, 0.000000000000000000 ) ) ;
#14058=ORIENTED_EDGE ( 'NONE', *, *, #5757, .T. ) ;
#14078=DIRECTION ( 'NONE',  ( 0.000000000000000000, 0.000000000000000000, 1.000000000000000000 ) ) ;
#14116=DIRECTION ( 'NONE',  ( -1.000000000000000000, -0.000000000000000000, -0.000000000000000000 ) ) ;
#14132=EDGE_CURVE ( 'NONE', #7721, #14191, #2829, .T. ) ;
#14136=EDGE_CURVE ( 'NONE', #4166, #5188, #3779, .T. ) ;
#14142=FACE_OUTER_BOUND ( 'NONE', #12795, .T. ) ;
#14156=CARTESIAN_POINT ( 'NONE',  ( 2.500000000000000000, -2.357898499370432166, 3.035766082959412415E-15 ) ) ;
#14164=ADVANCED_FACE ( 'NONE', ( #11610, #6964 ), #8072, .T. ) ;
#14165=VECTOR ( 'NONE', #12651, 1000.000000000000000 ) ;
#14191=VERTEX_POINT ( 'NONE', #13762 ) ;
#14202=DIRECTION ( 'NONE',  ( 0.000000000000000000, 0.000000000000000000, -1.000000000000000000 ) ) ;
#14209=EDGE_CURVE ( 'NONE', #8096, #5188, #4906, .T. ) ;
#14215=CARTESIAN_POINT ( 'NONE',  ( 2.500000000000000000, 1.768423874527823791, 1.020999999999998353 ) ) ;
#14224=AXIS2_PLACEMENT_3D ( 'NONE', #774, #5221, #2994 ) ;
#14238=CARTESIAN_POINT ( 'NONE',  ( 5.200000000000002842, 0.000000000000000000, 0.000000000000000000 ) ) ;
#14243=( LENGTH_UNIT ( ) NAMED_UNIT ( * ) SI_UNIT ( .MILLI., .METRE. ) );
#14253=DIRECTION ( 'NONE',  ( 0.000000000000000000, -0.5000000000000013323, -0.8660254037844380415 ) ) ;
#14294=EDGE_LOOP ( 'NONE', ( #2983, #4629, #12140 ) ) ;
#14302=DIRECTION ( 'NONE',  ( 0.000000000000000000, 0.000000000000000000, 1.000000000000000000 ) ) ;
#14317=EDGE_CURVE ( 'NONE', #8096, #1135, #12939, .T. ) ;
#14339=DIRECTION ( 'NONE',  ( -1.000000000000000000, -0.000000000000000000, -0.000000000000000000 ) ) ;
#14341=LINE ( 'NONE', #4235, #3505 ) ;
#14350=EDGE_CURVE ( 'NONE', #1573, #4609, #1180, .T. ) ;
#14367=ORIENTED_EDGE ( 'NONE', *, *, #14132, .T. ) ;
#14368=AXIS2_PLACEMENT_3D ( 'NONE', #1266, #2664, #10416 ) ;
#14371=DIRECTION ( 'NONE',  ( -1.000000000000000000, -0.000000000000000000, -0.000000000000000000 ) ) ;
#14403=EDGE_LOOP ( 'NONE', ( #13937, #6197, #13631, #8861, #6467 ) ) ;
#14422=AXIS2_PLACEMENT_3D ( 'NONE', #9998, #7787, #4388 ) ;
#14433=EDGE_CURVE ( 'NONE', #7000, #11781, #8106, .T. ) ;
#14434=CARTESIAN_POINT ( 'NONE',  ( 0.2500000000000002220, 4.898587196589412829E-16, -4.000000000000000000 ) ) ;
#14481=EDGE_CURVE ( 'NONE', #11591, #1324, #6856, .T. ) ;
#14483=VERTEX_POINT ( 'NONE', #6711 ) ;
#14506=EDGE_LOOP ( 'NONE', ( #6719, #1978, #1846, #12270, #10215 ) ) ;
#14527=DIRECTION ( 'NONE',  ( 0.000000000000000000, 0.000000000000000000, 1.000000000000000000 ) ) ;
#14533=CARTESIAN_POINT ( 'NONE',  ( 2.500000000000000000, 1.178949249685212974, -2.042000000000001148 ) ) ;
#14546=CARTESIAN_POINT ( 'NONE',  ( 2.500000000000000000, 2.357898499370431722, -2.818925648462311528E-15 ) ) ;
#14561=EDGE_CURVE ( 'NONE', #7721, #11030, #12982, .T. ) ;
#14588=AXIS2_PLACEMENT_3D ( 'NONE', #6214, #10932, #8572 ) ;
#14600=AXIS2_PLACEMENT_3D ( 'NONE', #4818, #4959, #10332 ) ;
#14675=COLOUR_RGB('Black',0.12,0.14,0.17);
#14676=FILL_AREA_STYLE_COLOUR('',#14675);
#14677=FILL_AREA_STYLE('',(#14676));
#14678=SURFACE_STYLE_FILL_AREA(#14677);
#14679=SURFACE_SIDE_STYLE('',(#14678));
#14680=SURFACE_STYLE_USAGE(.BOTH.,#14679);
#14681=PRESENTATION_STYLE_ASSIGNMENT((#14680));
ENDSEC;
END-ISO-10303-21;
